ISO-10303-21;
HEADER;
/* Generated by software containing ST-Developer
 * from STEP Tools, Inc. (www.steptools.com) 
 */

FILE_DESCRIPTION(
/* description */ ('Four-bar parallelogram arm'),
/* implementation_level */ '2;1');

FILE_NAME(
/* name */ 'M5x14 Cap Screw.step',
/* time_stamp */ '2026-10-28T03:24:55-07:00',
/* author */ (''),
/* organization */ (''),
/* preprocessor_version */ 'ST-DEVELOPER v20.2',
/* originating_system */ 'Autodesk Translation Framework v15.17.0.0',
/* authorisation */ '');

FILE_SCHEMA (('AUTOMOTIVE_DESIGN { 1 0 10303 214 3 1 1 }'));
ENDSEC;

DATA;
#10=MECHANICAL_DESIGN_GEOMETRIC_PRESENTATION_REPRESENTATION('',(#638),#14512);
#477=CONICAL_SURFACE('',#8197,0.4,0.785398163397448);
#478=CONICAL_SURFACE('',#8201,0.41,0.785398163397448);
#479=CONICAL_SURFACE('',#8205,0.26,0.463647609000806);
#491=ORIENTED_CLOSED_SHELL('',*,#7342,.F.);
#494=BREP_WITH_VOIDS('Body1',#7343,(#491));
#538=SHAPE_REPRESENTATION_RELATIONSHIP('SRR','None',#14759,#588);
#588=ADVANCED_BREP_SHAPE_REPRESENTATION('',(#494),#14474);
#638=STYLED_ITEM('',(#15094),#494);
#806=FACE_BOUND('',#1830,.T.);
#1078=PLANE('',#8185);
#1079=PLANE('',#8186);
#1080=PLANE('',#8187);
#1081=PLANE('',#8188);
#1082=PLANE('',#8189);
#1083=PLANE('',#8190);
#1084=PLANE('',#8191);
#1085=PLANE('',#8192);
#1086=PLANE('',#8193);
#1087=PLANE('',#8195);
#1088=PLANE('',#8203);
#1325=FACE_OUTER_BOUND('',#1816,.T.);
#1326=FACE_OUTER_BOUND('',#1817,.T.);
#1327=FACE_OUTER_BOUND('',#1818,.T.);
#1328=FACE_OUTER_BOUND('',#1819,.T.);
#1329=FACE_OUTER_BOUND('',#1820,.T.);
#1330=FACE_OUTER_BOUND('',#1821,.T.);
#1331=FACE_OUTER_BOUND('',#1822,.T.);
#1332=FACE_OUTER_BOUND('',#1823,.T.);
#1333=FACE_OUTER_BOUND('',#1824,.T.);
#1334=FACE_OUTER_BOUND('',#1825,.T.);
#1335=FACE_OUTER_BOUND('',#1826,.T.);
#1336=FACE_OUTER_BOUND('',#1827,.T.);
#1337=FACE_OUTER_BOUND('',#1828,.T.);
#1338=FACE_OUTER_BOUND('',#1829,.T.);
#1339=FACE_OUTER_BOUND('',#1831,.T.);
#1340=FACE_OUTER_BOUND('',#1832,.T.);
#1816=EDGE_LOOP('',(#5490,#5491,#5492,#5493));
#1817=EDGE_LOOP('',(#5494,#5495,#5496,#5497));
#1818=EDGE_LOOP('',(#5498,#5499,#5500,#5501));
#1819=EDGE_LOOP('',(#5502,#5503,#5504,#5505));
#1820=EDGE_LOOP('',(#5506,#5507,#5508,#5509));
#1821=EDGE_LOOP('',(#5510,#5511,#5512,#5513));
#1822=EDGE_LOOP('',(#5514,#5515,#5516,#5517,#5518,#5519));
#1823=EDGE_LOOP('',(#5520,#5521,#5522,#5523,#5524,#5525));
#1824=EDGE_LOOP('',(#5526));
#1825=EDGE_LOOP('',(#5527));
#1826=EDGE_LOOP('',(#5528,#5529,#5530,#5531));
#1827=EDGE_LOOP('',(#5532,#5533,#5534,#5535));
#1828=EDGE_LOOP('',(#5536,#5537,#5538,#5539));
#1829=EDGE_LOOP('',(#5540));
#1830=EDGE_LOOP('',(#5541));
#1831=EDGE_LOOP('',(#5542,#5543,#5544,#5545));
#1832=EDGE_LOOP('',(#5546,#5547,#5548,#5549));
#2452=LINE('',#12593,#2846);
#2453=LINE('',#12595,#2847);
#2454=LINE('',#12597,#2848);
#2455=LINE('',#12598,#2849);
#2456=LINE('',#12601,#2850);
#2457=LINE('',#12603,#2851);
#2458=LINE('',#12604,#2852);
#2459=LINE('',#12607,#2853);
#2460=LINE('',#12609,#2854);
#2461=LINE('',#12610,#2855);
#2462=LINE('',#12613,#2856);
#2463=LINE('',#12615,#2857);
#2464=LINE('',#12616,#2858);
#2465=LINE('',#12619,#2859);
#2466=LINE('',#12621,#2860);
#2467=LINE('',#12622,#2861);
#2468=LINE('',#12624,#2862);
#2469=LINE('',#12625,#2863);
#2470=LINE('',#12637,#2864);
#2471=LINE('',#12641,#2865);
#2472=LINE('',#12645,#2866);
#2473=LINE('',#12652,#2867);
#2474=LINE('',#12654,#2868);
#2846=VECTOR('',#9606,1.);
#2847=VECTOR('',#9607,1.);
#2848=VECTOR('',#9608,1.);
#2849=VECTOR('',#9609,1.);
#2850=VECTOR('',#9612,1.);
#2851=VECTOR('',#9613,1.);
#2852=VECTOR('',#9614,1.);
#2853=VECTOR('',#9617,1.);
#2854=VECTOR('',#9618,1.);
#2855=VECTOR('',#9619,1.);
#2856=VECTOR('',#9622,1.);
#2857=VECTOR('',#9623,1.);
#2858=VECTOR('',#9624,1.);
#2859=VECTOR('',#9627,1.);
#2860=VECTOR('',#9628,1.);
#2861=VECTOR('',#9629,1.);
#2862=VECTOR('',#9632,1.);
#2863=VECTOR('',#9633,1.);
#2864=VECTOR('',#9650,0.4);
#2865=VECTOR('',#9655,0.425);
#2866=VECTOR('',#9660,0.41);
#2867=VECTOR('',#9669,0.26);
#2868=VECTOR('',#9672,0.25);
#3205=CIRCLE('',#8194,0.24505);
#3206=CIRCLE('',#8196,0.375);
#3207=CIRCLE('',#8198,0.425);
#3208=CIRCLE('',#8200,0.425);
#3209=CIRCLE('',#8202,0.395);
#3210=CIRCLE('',#8204,0.27);
#3211=CIRCLE('',#8206,0.24505);
#3711=VERTEX_POINT('',#12591);
#3712=VERTEX_POINT('',#12592);
#3713=VERTEX_POINT('',#12594);
#3714=VERTEX_POINT('',#12596);
#3715=VERTEX_POINT('',#12600);
#3716=VERTEX_POINT('',#12602);
#3717=VERTEX_POINT('',#12606);
#3718=VERTEX_POINT('',#12608);
#3719=VERTEX_POINT('',#12612);
#3720=VERTEX_POINT('',#12614);
#3721=VERTEX_POINT('',#12618);
#3722=VERTEX_POINT('',#12620);
#3723=VERTEX_POINT('',#12629);
#3724=VERTEX_POINT('',#12632);
#3725=VERTEX_POINT('',#12635);
#3726=VERTEX_POINT('',#12639);
#3727=VERTEX_POINT('',#12643);
#3728=VERTEX_POINT('',#12647);
#3729=VERTEX_POINT('',#12650);
#4376=EDGE_CURVE('',#3711,#3712,#2452,.T.);
#4377=EDGE_CURVE('',#3712,#3713,#2453,.T.);
#4378=EDGE_CURVE('',#3713,#3714,#2454,.T.);
#4379=EDGE_CURVE('',#3711,#3714,#2455,.T.);
#4380=EDGE_CURVE('',#3712,#3715,#2456,.T.);
#4381=EDGE_CURVE('',#3715,#3716,#2457,.T.);
#4382=EDGE_CURVE('',#3716,#3713,#2458,.T.);
#4383=EDGE_CURVE('',#3715,#3717,#2459,.T.);
#4384=EDGE_CURVE('',#3717,#3718,#2460,.T.);
#4385=EDGE_CURVE('',#3718,#3716,#2461,.T.);
#4386=EDGE_CURVE('',#3717,#3719,#2462,.T.);
#4387=EDGE_CURVE('',#3719,#3720,#2463,.T.);
#4388=EDGE_CURVE('',#3720,#3718,#2464,.T.);
#4389=EDGE_CURVE('',#3719,#3721,#2465,.T.);
#4390=EDGE_CURVE('',#3721,#3722,#2466,.T.);
#4391=EDGE_CURVE('',#3722,#3720,#2467,.T.);
#4392=EDGE_CURVE('',#3721,#3711,#2468,.T.);
#4393=EDGE_CURVE('',#3714,#3722,#2469,.T.);
#4394=EDGE_CURVE('',#3723,#3723,#3205,.T.);
#4395=EDGE_CURVE('',#3724,#3724,#3206,.T.);
#4396=EDGE_CURVE('',#3725,#3725,#3207,.T.);
#4397=EDGE_CURVE('',#3725,#3724,#2470,.T.);
#4398=EDGE_CURVE('',#3726,#3726,#3208,.T.);
#4399=EDGE_CURVE('',#3726,#3725,#2471,.T.);
#4400=EDGE_CURVE('',#3727,#3727,#3209,.T.);
#4401=EDGE_CURVE('',#3727,#3726,#2472,.T.);
#4402=EDGE_CURVE('',#3728,#3728,#3210,.T.);
#4403=EDGE_CURVE('',#3729,#3729,#3211,.F.);
#4404=EDGE_CURVE('',#3729,#3728,#2473,.T.);
#4405=EDGE_CURVE('',#3723,#3729,#2474,.T.);
#5490=ORIENTED_EDGE('',*,*,#4376,.T.);
#5491=ORIENTED_EDGE('',*,*,#4377,.T.);
#5492=ORIENTED_EDGE('',*,*,#4378,.T.);
#5493=ORIENTED_EDGE('',*,*,#4379,.F.);
#5494=ORIENTED_EDGE('',*,*,#4380,.T.);
#5495=ORIENTED_EDGE('',*,*,#4381,.T.);
#5496=ORIENTED_EDGE('',*,*,#4382,.T.);
#5497=ORIENTED_EDGE('',*,*,#4377,.F.);
#5498=ORIENTED_EDGE('',*,*,#4383,.T.);
#5499=ORIENTED_EDGE('',*,*,#4384,.T.);
#5500=ORIENTED_EDGE('',*,*,#4385,.T.);
#5501=ORIENTED_EDGE('',*,*,#4381,.F.);
#5502=ORIENTED_EDGE('',*,*,#4386,.T.);
#5503=ORIENTED_EDGE('',*,*,#4387,.T.);
#5504=ORIENTED_EDGE('',*,*,#4388,.T.);
#5505=ORIENTED_EDGE('',*,*,#4384,.F.);
#5506=ORIENTED_EDGE('',*,*,#4389,.T.);
#5507=ORIENTED_EDGE('',*,*,#4390,.T.);
#5508=ORIENTED_EDGE('',*,*,#4391,.T.);
#5509=ORIENTED_EDGE('',*,*,#4387,.F.);
#5510=ORIENTED_EDGE('',*,*,#4392,.T.);
#5511=ORIENTED_EDGE('',*,*,#4379,.T.);
#5512=ORIENTED_EDGE('',*,*,#4393,.T.);
#5513=ORIENTED_EDGE('',*,*,#4390,.F.);
#5514=ORIENTED_EDGE('',*,*,#4392,.F.);
#5515=ORIENTED_EDGE('',*,*,#4389,.F.);
#5516=ORIENTED_EDGE('',*,*,#4386,.F.);
#5517=ORIENTED_EDGE('',*,*,#4383,.F.);
#5518=ORIENTED_EDGE('',*,*,#4380,.F.);
#5519=ORIENTED_EDGE('',*,*,#4376,.F.);
#5520=ORIENTED_EDGE('',*,*,#4393,.F.);
#5521=ORIENTED_EDGE('',*,*,#4378,.F.);
#5522=ORIENTED_EDGE('',*,*,#4382,.F.);
#5523=ORIENTED_EDGE('',*,*,#4385,.F.);
#5524=ORIENTED_EDGE('',*,*,#4388,.F.);
#5525=ORIENTED_EDGE('',*,*,#4391,.F.);
#5526=ORIENTED_EDGE('',*,*,#4394,.F.);
#5527=ORIENTED_EDGE('',*,*,#4395,.F.);
#5528=ORIENTED_EDGE('',*,*,#4396,.F.);
#5529=ORIENTED_EDGE('',*,*,#4397,.T.);
#5530=ORIENTED_EDGE('',*,*,#4395,.T.);
#5531=ORIENTED_EDGE('',*,*,#4397,.F.);
#5532=ORIENTED_EDGE('',*,*,#4398,.F.);
#5533=ORIENTED_EDGE('',*,*,#4399,.T.);
#5534=ORIENTED_EDGE('',*,*,#4396,.T.);
#5535=ORIENTED_EDGE('',*,*,#4399,.F.);
#5536=ORIENTED_EDGE('',*,*,#4400,.F.);
#5537=ORIENTED_EDGE('',*,*,#4401,.T.);
#5538=ORIENTED_EDGE('',*,*,#4398,.T.);
#5539=ORIENTED_EDGE('',*,*,#4401,.F.);
#5540=ORIENTED_EDGE('',*,*,#4400,.T.);
#5541=ORIENTED_EDGE('',*,*,#4402,.F.);
#5542=ORIENTED_EDGE('',*,*,#4403,.F.);
#5543=ORIENTED_EDGE('',*,*,#4404,.T.);
#5544=ORIENTED_EDGE('',*,*,#4402,.T.);
#5545=ORIENTED_EDGE('',*,*,#4404,.F.);
#5546=ORIENTED_EDGE('',*,*,#4394,.T.);
#5547=ORIENTED_EDGE('',*,*,#4405,.T.);
#5548=ORIENTED_EDGE('',*,*,#4403,.T.);
#5549=ORIENTED_EDGE('',*,*,#4405,.F.);
#6765=CYLINDRICAL_SURFACE('',#8199,0.425);
#6766=CYLINDRICAL_SURFACE('',#8207,0.24505);
#7030=ADVANCED_FACE('',(#1325),#1078,.F.);
#7031=ADVANCED_FACE('',(#1326),#1079,.F.);
#7032=ADVANCED_FACE('',(#1327),#1080,.F.);
#7033=ADVANCED_FACE('',(#1328),#1081,.F.);
#7034=ADVANCED_FACE('',(#1329),#1082,.F.);
#7035=ADVANCED_FACE('',(#1330),#1083,.F.);
#7036=ADVANCED_FACE('',(#1331),#1084,.F.);
#7037=ADVANCED_FACE('',(#1332),#1085,.F.);
#7038=ADVANCED_FACE('',(#1333),#1086,.F.);
#7039=ADVANCED_FACE('',(#1334),#1087,.T.);
#7040=ADVANCED_FACE('',(#1335),#477,.T.);
#7041=ADVANCED_FACE('',(#1336),#6765,.T.);
#7042=ADVANCED_FACE('',(#1337),#478,.T.);
#7043=ADVANCED_FACE('',(#1338,#806),#1088,.T.);
#7044=ADVANCED_FACE('',(#1339),#479,.T.);
#7045=ADVANCED_FACE('',(#1340),#6766,.T.);
#7342=CLOSED_SHELL('',(#7030,#7031,#7032,#7033,#7034,#7035,#7036,#7037));
#7343=CLOSED_SHELL('',(#7038,#7039,#7040,#7041,#7042,#7043,#7044,#7045));
#8184=AXIS2_PLACEMENT_3D('',#12589,#9602,#9603);
#8185=AXIS2_PLACEMENT_3D('',#12590,#9604,#9605);
#8186=AXIS2_PLACEMENT_3D('',#12599,#9610,#9611);
#8187=AXIS2_PLACEMENT_3D('',#12605,#9615,#9616);
#8188=AXIS2_PLACEMENT_3D('',#12611,#9620,#9621);
#8189=AXIS2_PLACEMENT_3D('',#12617,#9625,#9626);
#8190=AXIS2_PLACEMENT_3D('',#12623,#9630,#9631);
#8191=AXIS2_PLACEMENT_3D('',#12626,#9634,#9635);
#8192=AXIS2_PLACEMENT_3D('',#12627,#9636,#9637);
#8193=AXIS2_PLACEMENT_3D('',#12628,#9638,#9639);
#8194=AXIS2_PLACEMENT_3D('',#12630,#9640,#9641);
#8195=AXIS2_PLACEMENT_3D('',#12631,#9642,#9643);
#8196=AXIS2_PLACEMENT_3D('',#12633,#9644,#9645);
#8197=AXIS2_PLACEMENT_3D('',#12634,#9646,#9647);
#8198=AXIS2_PLACEMENT_3D('',#12636,#9648,#9649);
#8199=AXIS2_PLACEMENT_3D('',#12638,#9651,#9652);
#8200=AXIS2_PLACEMENT_3D('',#12640,#9653,#9654);
#8201=AXIS2_PLACEMENT_3D('',#12642,#9656,#9657);
#8202=AXIS2_PLACEMENT_3D('',#12644,#9658,#9659);
#8203=AXIS2_PLACEMENT_3D('',#12646,#9661,#9662);
#8204=AXIS2_PLACEMENT_3D('',#12648,#9663,#9664);
#8205=AXIS2_PLACEMENT_3D('',#12649,#9665,#9666);
#8206=AXIS2_PLACEMENT_3D('',#12651,#9667,#9668);
#8207=AXIS2_PLACEMENT_3D('',#12653,#9670,#9671);
#9602=DIRECTION('axis',(0.,0.,1.));
#9603=DIRECTION('refdir',(1.,0.,0.));
#9604=DIRECTION('center_axis',(0.866025403784439,0.,-0.5));
#9605=DIRECTION('ref_axis',(0.5,0.,0.866025403784439));
#9606=DIRECTION('',(-0.5,0.,-0.866025403784439));
#9607=DIRECTION('',(0.,-1.,0.));
#9608=DIRECTION('',(0.5,0.,0.866025403784439));
#9609=DIRECTION('',(0.,-1.,0.));
#9610=DIRECTION('center_axis',(1.20185167898973E-16,0.,-1.));
#9611=DIRECTION('ref_axis',(1.,0.,1.20185167898973E-16));
#9612=DIRECTION('',(-1.,0.,-1.20185167898973E-16));
#9613=DIRECTION('',(0.,-1.,0.));
#9614=DIRECTION('',(1.,0.,1.20185167898973E-16));
#9615=DIRECTION('center_axis',(-0.866025403784439,0.,-0.5));
#9616=DIRECTION('ref_axis',(0.5,0.,-0.866025403784439));
#9617=DIRECTION('',(-0.5,0.,0.866025403784439));
#9618=DIRECTION('',(0.,-1.,0.));
#9619=DIRECTION('',(0.5,0.,-0.866025403784439));
#9620=DIRECTION('center_axis',(-0.866025403784439,0.,0.5));
#9621=DIRECTION('ref_axis',(-0.5,0.,-0.866025403784439));
#9622=DIRECTION('',(0.5,0.,0.866025403784439));
#9623=DIRECTION('',(0.,-1.,0.));
#9624=DIRECTION('',(-0.5,0.,-0.866025403784439));
#9625=DIRECTION('center_axis',(-2.40370335797945E-16,0.,1.));
#9626=DIRECTION('ref_axis',(-1.,0.,-2.40370335797945E-16));
#9627=DIRECTION('',(1.,0.,2.40370335797945E-16));
#9628=DIRECTION('',(0.,-1.,0.));
#9629=DIRECTION('',(-1.,0.,-2.40370335797945E-16));
#9630=DIRECTION('center_axis',(0.866025403784439,0.,0.5));
#9631=DIRECTION('ref_axis',(-0.5,0.,0.866025403784439));
#9632=DIRECTION('',(0.5,0.,-0.866025403784439));
#9633=DIRECTION('',(-0.5,0.,0.866025403784439));
#9634=DIRECTION('center_axis',(0.,1.,0.));
#9635=DIRECTION('ref_axis',(1.,0.,0.));
#9636=DIRECTION('center_axis',(0.,-1.,0.));
#9637=DIRECTION('ref_axis',(0.,0.,-1.));
#9638=DIRECTION('center_axis',(0.,1.,0.));
#9639=DIRECTION('ref_axis',(1.,0.,0.));
#9640=DIRECTION('center_axis',(0.,1.,0.));
#9641=DIRECTION('ref_axis',(1.,0.,0.));
#9642=DIRECTION('center_axis',(0.,1.,0.));
#9643=DIRECTION('ref_axis',(0.,0.,1.));
#9644=DIRECTION('center_axis',(0.,-1.,0.));
#9645=DIRECTION('ref_axis',(1.,0.,0.));
#9646=DIRECTION('center_axis',(0.,-1.,0.));
#9647=DIRECTION('ref_axis',(1.,0.,0.));
#9648=DIRECTION('center_axis',(0.,-1.,0.));
#9649=DIRECTION('ref_axis',(1.,0.,0.));
#9650=DIRECTION('',(0.707106781186548,0.707106781186547,8.65956056235493E-17));
#9651=DIRECTION('center_axis',(0.,-1.,0.));
#9652=DIRECTION('ref_axis',(1.,0.,0.));
#9653=DIRECTION('center_axis',(0.,-1.,0.));
#9654=DIRECTION('ref_axis',(1.,0.,0.));
#9655=DIRECTION('',(0.,1.,0.));
#9656=DIRECTION('center_axis',(0.,1.,0.));
#9657=DIRECTION('ref_axis',(1.,0.,0.));
#9658=DIRECTION('center_axis',(0.,-1.,0.));
#9659=DIRECTION('ref_axis',(1.,0.,0.));
#9660=DIRECTION('',(-0.707106781186547,0.707106781186548,-8.65956056235493E-17));
#9661=DIRECTION('center_axis',(0.,-1.,0.));
#9662=DIRECTION('ref_axis',(0.,0.,-1.));
#9663=DIRECTION('center_axis',(0.,-1.,0.));
#9664=DIRECTION('ref_axis',(1.,0.,0.));
#9665=DIRECTION('center_axis',(0.,1.,0.));
#9666=DIRECTION('ref_axis',(1.,0.,0.));
#9667=DIRECTION('center_axis',(0.,1.,0.));
#9668=DIRECTION('ref_axis',(1.,0.,0.));
#9669=DIRECTION('',(-0.447213595499958,0.894427190999916,-5.47678698264203E-17));
#9670=DIRECTION('center_axis',(0.,-1.,0.));
#9671=DIRECTION('ref_axis',(1.,0.,0.));
#9672=DIRECTION('',(0.,1.,0.));
#12589=CARTESIAN_POINT('',(0.,0.,0.));
#12590=CARTESIAN_POINT('Origin',(0.115470053837925,-0.5,-0.2));
#12591=CARTESIAN_POINT('',(0.23094010767585,-0.5,0.));
#12592=CARTESIAN_POINT('',(0.115470053837925,-0.5,-0.2));
#12593=CARTESIAN_POINT('',(0.23094010767585,-0.5,0.));
#12594=CARTESIAN_POINT('',(0.115470053837925,-0.8,-0.2));
#12595=CARTESIAN_POINT('',(0.115470053837925,-0.5,-0.2));
#12596=CARTESIAN_POINT('',(0.23094010767585,-0.8,0.));
#12597=CARTESIAN_POINT('',(0.23094010767585,-0.8,0.));
#12598=CARTESIAN_POINT('',(0.23094010767585,-0.5,0.));
#12599=CARTESIAN_POINT('Origin',(-0.115470053837925,-0.5,-0.2));
#12600=CARTESIAN_POINT('',(-0.115470053837925,-0.5,-0.2));
#12601=CARTESIAN_POINT('',(0.115470053837925,-0.5,-0.2));
#12602=CARTESIAN_POINT('',(-0.115470053837925,-0.8,-0.2));
#12603=CARTESIAN_POINT('',(-0.115470053837925,-0.5,-0.2));
#12604=CARTESIAN_POINT('',(0.115470053837925,-0.8,-0.2));
#12605=CARTESIAN_POINT('Origin',(-0.23094010767585,-0.5,-2.77555756156289E-17));
#12606=CARTESIAN_POINT('',(-0.23094010767585,-0.5,-2.82820063659975E-17));
#12607=CARTESIAN_POINT('',(-0.115470053837925,-0.5,-0.2));
#12608=CARTESIAN_POINT('',(-0.23094010767585,-0.8,-2.77555756156289E-17));
#12609=CARTESIAN_POINT('',(-0.23094010767585,-0.5,-2.82820063659975E-17));
#12610=CARTESIAN_POINT('',(-0.115470053837925,-0.8,-0.2));
#12611=CARTESIAN_POINT('Origin',(-0.115470053837925,-0.5,0.2));
#12612=CARTESIAN_POINT('',(-0.115470053837925,-0.5,0.2));
#12613=CARTESIAN_POINT('',(-0.23094010767585,-0.5,-2.82820063659975E-17));
#12614=CARTESIAN_POINT('',(-0.115470053837925,-0.8,0.2));
#12615=CARTESIAN_POINT('',(-0.115470053837925,-0.5,0.2));
#12616=CARTESIAN_POINT('',(-0.23094010767585,-0.8,-2.82820063659975E-17));
#12617=CARTESIAN_POINT('Origin',(0.115470053837925,-0.5,0.2));
#12618=CARTESIAN_POINT('',(0.115470053837925,-0.5,0.2));
#12619=CARTESIAN_POINT('',(-0.115470053837925,-0.5,0.2));
#12620=CARTESIAN_POINT('',(0.115470053837925,-0.8,0.2));
#12621=CARTESIAN_POINT('',(0.115470053837925,-0.5,0.2));
#12622=CARTESIAN_POINT('',(-0.115470053837925,-0.8,0.2));
#12623=CARTESIAN_POINT('Origin',(0.23094010767585,-0.5,0.));
#12624=CARTESIAN_POINT('',(0.115470053837925,-0.5,0.2));
#12625=CARTESIAN_POINT('',(0.115470053837925,-0.8,0.2));
#12626=CARTESIAN_POINT('Origin',(0.,-0.5,0.));
#12627=CARTESIAN_POINT('Origin',(0.,-0.8,0.));
#12628=CARTESIAN_POINT('Origin',(0.,-1.4,0.));
#12629=CARTESIAN_POINT('',(-0.24505,-1.4,3.00099698131059E-17));
#12630=CARTESIAN_POINT('Origin',(0.,-1.4,0.));
#12631=CARTESIAN_POINT('Origin',(0.375,0.5,0.));
#12632=CARTESIAN_POINT('',(-0.375,0.5,-4.59242549680257E-17));
#12633=CARTESIAN_POINT('Origin',(0.,0.5,0.));
#12634=CARTESIAN_POINT('Origin',(0.,0.475,0.));
#12635=CARTESIAN_POINT('',(-0.425,0.45,-5.20474889637625E-17));
#12636=CARTESIAN_POINT('Origin',(0.,0.45,0.));
#12637=CARTESIAN_POINT('',(-0.4,0.475,-4.89858719658941E-17));
#12638=CARTESIAN_POINT('Origin',(0.,0.24,0.));
#12639=CARTESIAN_POINT('',(-0.425,0.0299999999999998,-5.20474889637625E-17));
#12640=CARTESIAN_POINT('Origin',(0.,0.0299999999999998,0.));
#12641=CARTESIAN_POINT('',(-0.425,0.24,-5.20474889637625E-17));
#12642=CARTESIAN_POINT('Origin',(0.,0.0150000000000001,0.));
#12643=CARTESIAN_POINT('',(-0.395,4.85722573273506E-17,-4.83735485663204E-17));
#12644=CARTESIAN_POINT('Origin',(0.,0.,0.));
#12645=CARTESIAN_POINT('',(-0.41,0.0150000000000001,-5.02105187650415E-17));
#12646=CARTESIAN_POINT('Origin',(0.27,0.,0.));
#12647=CARTESIAN_POINT('',(-0.27,0.,-3.30654635769785E-17));
#12648=CARTESIAN_POINT('Origin',(0.,0.,0.));
#12649=CARTESIAN_POINT('Origin',(0.,-0.02,0.));
#12650=CARTESIAN_POINT('',(-0.24505,-0.0498999999999999,3.00099698131059E-17));
#12651=CARTESIAN_POINT('Origin',(0.,-0.0498999999999999,0.));
#12652=CARTESIAN_POINT('',(-0.26,-0.02,-3.18408167778312E-17));
#12653=CARTESIAN_POINT('Origin',(0.,-0.995,0.));
#12654=CARTESIAN_POINT('',(-0.24505,-0.995,-3.00099698131059E-17));
#14417=UNCERTAINTY_MEASURE_WITH_UNIT(LENGTH_MEASURE(0.001),#14513,
'DISTANCE_ACCURACY_VALUE',
'Maximum model space distance between geometric entities at asserted c
onnectivities');
#14455=UNCERTAINTY_MEASURE_WITH_UNIT(LENGTH_MEASURE(0.001),#14513,
'DISTANCE_ACCURACY_VALUE',
'Maximum model space distance between geometric entities at asserted c
onnectivities');
#14474=(
GEOMETRIC_REPRESENTATION_CONTEXT(3)
GLOBAL_UNCERTAINTY_ASSIGNED_CONTEXT((#14417))
GLOBAL_UNIT_ASSIGNED_CONTEXT((#14513,#14515,#14516))
REPRESENTATION_CONTEXT('','3D')
);
#14512=(
GEOMETRIC_REPRESENTATION_CONTEXT(3)
GLOBAL_UNCERTAINTY_ASSIGNED_CONTEXT((#14455))
GLOBAL_UNIT_ASSIGNED_CONTEXT((#14513,#14515,#14516))
REPRESENTATION_CONTEXT('','3D')
);
#14513=(
LENGTH_UNIT()
NAMED_UNIT(*)
SI_UNIT(.CENTI.,.METRE.)
);
#14515=(
NAMED_UNIT(*)
PLANE_ANGLE_UNIT()
SI_UNIT($,.RADIAN.)
);
#14516=(
NAMED_UNIT(*)
SI_UNIT($,.STERADIAN.)
SOLID_ANGLE_UNIT()
);
#14535=SHAPE_DEFINITION_REPRESENTATION(#14591,#14759);
#14591=PRODUCT_DEFINITION_SHAPE('',$,#14816);
#14759=SHAPE_REPRESENTATION('',(#8184),#14474);
#14797=PRODUCT_DEFINITION_CONTEXT('part definition',#14967,'design');
#14816=PRODUCT_DEFINITION('M5x14 Cap Screw','M5x14 Cap Screw',#14872,#14797);
#14872=PRODUCT_DEFINITION_FORMATION('',$,#14987);
#14967=APPLICATION_CONTEXT(
'Core Data for Automotive Mechanical Design Process');
#14968=PRODUCT_CONTEXT('part definition',#14967,'mechanical');
#14987=PRODUCT('M5x14 Cap Screw','M5x14 Cap Screw','M5x14 Cap Screw',(#14968));
#15088=COLOUR_RGB('Black',0.12,0.14,0.17);
#15089=FILL_AREA_STYLE_COLOUR('',#15088);
#15090=FILL_AREA_STYLE('',(#15089));
#15091=SURFACE_STYLE_FILL_AREA(#15090);
#15092=SURFACE_SIDE_STYLE('',(#15091));
#15093=SURFACE_STYLE_USAGE(.BOTH.,#15092);
#15094=PRESENTATION_STYLE_ASSIGNMENT((#15093));
ENDSEC;
END-ISO-10303-21;
